ISO-10303-21;
HEADER;
/* Generated by software containing ST-Developer
 * from STEP Tools, Inc. (www.steptools.com) 
 */

FILE_DESCRIPTION(
/* description */ ('Hook toggle clamp'),
/* implementation_level */ '2;1');

FILE_NAME(
/* name */ 'Hex Nut - M8.step',
/* time_stamp */ '2026-10-27T21:56:56-07:00',
/* author */ (''),
/* organization */ (''),
/* preprocessor_version */ 'ST-DEVELOPER v20.2',
/* originating_system */ 'Autodesk Translation Framework v15.17.0.0',
/* authorisation */ '');

FILE_SCHEMA (('AUTOMOTIVE_DESIGN { 1 0 10303 214 3 1 1 }'));
ENDSEC;

DATA;
#10=MECHANICAL_DESIGN_GEOMETRIC_PRESENTATION_REPRESENTATION('',(#205),#5458);
#135=(
BOUNDED_CURVE()
B_SPLINE_CURVE(2,(#5327,#5328,#5329),.UNSPECIFIED.,.F.,.F.)
B_SPLINE_CURVE_WITH_KNOTS((3,3),(0.14973948338295,0.97160236658079),
 .UNSPECIFIED.)
CURVE()
GEOMETRIC_REPRESENTATION_ITEM()
RATIONAL_B_SPLINE_CURVE((1.07140024848292,1.23714644374248,1.07140024848292))
REPRESENTATION_ITEM('')
);
#136=(
BOUNDED_CURVE()
B_SPLINE_CURVE(2,(#5331,#5332,#5333),.UNSPECIFIED.,.F.,.F.)
B_SPLINE_CURVE_WITH_KNOTS((3,3),(0.14973948338295,0.971602366580789),
 .UNSPECIFIED.)
CURVE()
GEOMETRIC_REPRESENTATION_ITEM()
RATIONAL_B_SPLINE_CURVE((1.07140024848292,1.23714644374248,1.07140024848292))
REPRESENTATION_ITEM('')
);
#137=(
BOUNDED_CURVE()
B_SPLINE_CURVE(2,(#5338,#5339,#5340),.UNSPECIFIED.,.F.,.F.)
B_SPLINE_CURVE_WITH_KNOTS((3,3),(0.14973948338295,0.97160236658079),
 .UNSPECIFIED.)
CURVE()
GEOMETRIC_REPRESENTATION_ITEM()
RATIONAL_B_SPLINE_CURVE((1.07140024848292,1.23714644374248,1.07140024848292))
REPRESENTATION_ITEM('')
);
#138=(
BOUNDED_CURVE()
B_SPLINE_CURVE(2,(#5342,#5343,#5344),.UNSPECIFIED.,.F.,.F.)
B_SPLINE_CURVE_WITH_KNOTS((3,3),(0.14973948338295,0.97160236658079),
 .UNSPECIFIED.)
CURVE()
GEOMETRIC_REPRESENTATION_ITEM()
RATIONAL_B_SPLINE_CURVE((1.07140024848292,1.23714644374248,1.07140024848292))
REPRESENTATION_ITEM('')
);
#139=(
BOUNDED_CURVE()
B_SPLINE_CURVE(2,(#5346,#5347,#5348),.UNSPECIFIED.,.F.,.F.)
B_SPLINE_CURVE_WITH_KNOTS((3,3),(0.14973948338295,0.971602366580789),
 .UNSPECIFIED.)
CURVE()
GEOMETRIC_REPRESENTATION_ITEM()
RATIONAL_B_SPLINE_CURVE((1.07140024848292,1.23714644374248,1.07140024848292))
REPRESENTATION_ITEM('')
);
#140=(
BOUNDED_CURVE()
B_SPLINE_CURVE(2,(#5349,#5350,#5351),.UNSPECIFIED.,.F.,.F.)
B_SPLINE_CURVE_WITH_KNOTS((3,3),(0.14973948338295,0.97160236658079),
 .UNSPECIFIED.)
CURVE()
GEOMETRIC_REPRESENTATION_ITEM()
RATIONAL_B_SPLINE_CURVE((1.07140024848292,1.23714644374248,1.07140024848292))
REPRESENTATION_ITEM('')
);
#141=(
BOUNDED_CURVE()
B_SPLINE_CURVE(2,(#5358,#5359,#5360),.UNSPECIFIED.,.F.,.F.)
B_SPLINE_CURVE_WITH_KNOTS((3,3),(0.14973948338295,0.97160236658079),
 .UNSPECIFIED.)
CURVE()
GEOMETRIC_REPRESENTATION_ITEM()
RATIONAL_B_SPLINE_CURVE((1.07140024848292,1.23714644374248,1.07140024848292))
REPRESENTATION_ITEM('')
);
#142=(
BOUNDED_CURVE()
B_SPLINE_CURVE(2,(#5362,#5363,#5364),.UNSPECIFIED.,.F.,.F.)
B_SPLINE_CURVE_WITH_KNOTS((3,3),(0.14973948338295,0.97160236658079),
 .UNSPECIFIED.)
CURVE()
GEOMETRIC_REPRESENTATION_ITEM()
RATIONAL_B_SPLINE_CURVE((1.07140024848292,1.23714644374248,1.07140024848292))
REPRESENTATION_ITEM('')
);
#143=(
BOUNDED_CURVE()
B_SPLINE_CURVE(2,(#5366,#5367,#5368),.UNSPECIFIED.,.F.,.F.)
B_SPLINE_CURVE_WITH_KNOTS((3,3),(0.14973948338295,0.971602366580789),
 .UNSPECIFIED.)
CURVE()
GEOMETRIC_REPRESENTATION_ITEM()
RATIONAL_B_SPLINE_CURVE((1.07140024848292,1.23714644374248,1.07140024848292))
REPRESENTATION_ITEM('')
);
#144=(
BOUNDED_CURVE()
B_SPLINE_CURVE(2,(#5370,#5371,#5372),.UNSPECIFIED.,.F.,.F.)
B_SPLINE_CURVE_WITH_KNOTS((3,3),(0.14973948338295,0.97160236658079),
 .UNSPECIFIED.)
CURVE()
GEOMETRIC_REPRESENTATION_ITEM()
RATIONAL_B_SPLINE_CURVE((1.07140024848292,1.23714644374248,1.07140024848292))
REPRESENTATION_ITEM('')
);
#145=(
BOUNDED_CURVE()
B_SPLINE_CURVE(2,(#5374,#5375,#5376),.UNSPECIFIED.,.F.,.F.)
B_SPLINE_CURVE_WITH_KNOTS((3,3),(0.14973948338295,0.97160236658079),
 .UNSPECIFIED.)
CURVE()
GEOMETRIC_REPRESENTATION_ITEM()
RATIONAL_B_SPLINE_CURVE((1.07140024848292,1.23714644374248,1.07140024848292))
REPRESENTATION_ITEM('')
);
#146=(
BOUNDED_CURVE()
B_SPLINE_CURVE(2,(#5377,#5378,#5379),.UNSPECIFIED.,.F.,.F.)
B_SPLINE_CURVE_WITH_KNOTS((3,3),(0.14973948338295,0.971602366580789),
 .UNSPECIFIED.)
CURVE()
GEOMETRIC_REPRESENTATION_ITEM()
RATIONAL_B_SPLINE_CURVE((1.07140024848292,1.23714644374248,1.07140024848292))
REPRESENTATION_ITEM('')
);
#153=CONICAL_SURFACE('',#3483,0.734027674973257,1.0471975511966);
#154=CONICAL_SURFACE('',#3485,0.734027674973257,1.0471975511966);
#171=SHAPE_REPRESENTATION_RELATIONSHIP('SRR','None',#5555,#188);
#188=ADVANCED_BREP_SHAPE_REPRESENTATION('',(#221),#5457);
#205=STYLED_ITEM('',(#5724),#221);
#221=MANIFOLD_SOLID_BREP('Body1',#2987);
#276=FACE_BOUND('',#792,.T.);
#277=FACE_BOUND('',#794,.T.);
#385=PLANE('',#3487);
#386=PLANE('',#3488);
#387=PLANE('',#3489);
#388=PLANE('',#3493);
#389=PLANE('',#3494);
#390=PLANE('',#3495);
#391=PLANE('',#3496);
#392=PLANE('',#3497);
#555=FACE_OUTER_BOUND('',#782,.T.);
#556=FACE_OUTER_BOUND('',#783,.T.);
#557=FACE_OUTER_BOUND('',#784,.T.);
#558=FACE_OUTER_BOUND('',#785,.T.);
#559=FACE_OUTER_BOUND('',#786,.T.);
#560=FACE_OUTER_BOUND('',#787,.T.);
#561=FACE_OUTER_BOUND('',#788,.T.);
#562=FACE_OUTER_BOUND('',#789,.T.);
#563=FACE_OUTER_BOUND('',#790,.T.);
#564=FACE_OUTER_BOUND('',#791,.T.);
#565=FACE_OUTER_BOUND('',#793,.T.);
#782=EDGE_LOOP('',(#2699,#2700,#2701,#2702,#2703,#2704,#2705,#2706,#2707));
#783=EDGE_LOOP('',(#2708,#2709,#2710,#2711,#2712,#2713,#2714,#2715,#2716));
#784=EDGE_LOOP('',(#2717,#2718,#2719,#2720));
#785=EDGE_LOOP('',(#2721,#2722,#2723,#2724));
#786=EDGE_LOOP('',(#2725,#2726,#2727,#2728));
#787=EDGE_LOOP('',(#2729,#2730,#2731,#2732));
#788=EDGE_LOOP('',(#2733,#2734,#2735,#2736));
#789=EDGE_LOOP('',(#2737,#2738,#2739,#2740));
#790=EDGE_LOOP('',(#2741,#2742,#2743,#2744));
#791=EDGE_LOOP('',(#2745));
#792=EDGE_LOOP('',(#2746));
#793=EDGE_LOOP('',(#2747));
#794=EDGE_LOOP('',(#2748));
#1023=LINE('',#5335,#1260);
#1024=LINE('',#5356,#1261);
#1025=LINE('',#5381,#1262);
#1026=LINE('',#5382,#1263);
#1027=LINE('',#5384,#1264);
#1028=LINE('',#5386,#1265);
#1029=LINE('',#5391,#1266);
#1030=LINE('',#5394,#1267);
#1031=LINE('',#5396,#1268);
#1260=VECTOR('',#4355,0.734027674973257);
#1261=VECTOR('',#4362,0.734027674973257);
#1262=VECTOR('',#4365,1.);
#1263=VECTOR('',#4366,1.);
#1264=VECTOR('',#4369,1.);
#1265=VECTOR('',#4372,1.);
#1266=VECTOR('',#4377,0.4);
#1267=VECTOR('',#4382,1.);
#1268=VECTOR('',#4385,1.);
#1378=CIRCLE('',#3484,0.6175);
#1379=CIRCLE('',#3486,0.6175);
#1380=CIRCLE('',#3491,0.338975);
#1381=CIRCLE('',#3492,0.338975);
#1611=VERTEX_POINT('',#5325);
#1612=VERTEX_POINT('',#5326);
#1613=VERTEX_POINT('',#5330);
#1614=VERTEX_POINT('',#5334);
#1615=VERTEX_POINT('',#5337);
#1616=VERTEX_POINT('',#5341);
#1617=VERTEX_POINT('',#5345);
#1618=VERTEX_POINT('',#5353);
#1619=VERTEX_POINT('',#5355);
#1620=VERTEX_POINT('',#5357);
#1621=VERTEX_POINT('',#5361);
#1622=VERTEX_POINT('',#5365);
#1623=VERTEX_POINT('',#5369);
#1624=VERTEX_POINT('',#5373);
#1625=VERTEX_POINT('',#5388);
#1626=VERTEX_POINT('',#5390);
#1976=EDGE_CURVE('',#1611,#1612,#135,.T.);
#1977=EDGE_CURVE('',#1613,#1611,#136,.T.);
#1978=EDGE_CURVE('',#1613,#1614,#1023,.T.);
#1979=EDGE_CURVE('',#1614,#1614,#1378,.T.);
#1980=EDGE_CURVE('',#1615,#1613,#137,.T.);
#1981=EDGE_CURVE('',#1616,#1615,#138,.T.);
#1982=EDGE_CURVE('',#1617,#1616,#139,.T.);
#1983=EDGE_CURVE('',#1612,#1617,#140,.T.);
#1984=EDGE_CURVE('',#1618,#1618,#1379,.T.);
#1985=EDGE_CURVE('',#1618,#1619,#1024,.T.);
#1986=EDGE_CURVE('',#1620,#1619,#141,.T.);
#1987=EDGE_CURVE('',#1621,#1620,#142,.T.);
#1988=EDGE_CURVE('',#1622,#1621,#143,.T.);
#1989=EDGE_CURVE('',#1623,#1622,#144,.T.);
#1990=EDGE_CURVE('',#1624,#1623,#145,.T.);
#1991=EDGE_CURVE('',#1619,#1624,#146,.T.);
#1992=EDGE_CURVE('',#1615,#1624,#1025,.T.);
#1993=EDGE_CURVE('',#1616,#1623,#1026,.T.);
#1994=EDGE_CURVE('',#1613,#1619,#1027,.T.);
#1995=EDGE_CURVE('',#1611,#1620,#1028,.T.);
#1996=EDGE_CURVE('',#1625,#1625,#1380,.F.);
#1997=EDGE_CURVE('',#1625,#1626,#1029,.T.);
#1998=EDGE_CURVE('',#1626,#1626,#1381,.F.);
#1999=EDGE_CURVE('',#1612,#1621,#1030,.T.);
#2000=EDGE_CURVE('',#1617,#1622,#1031,.T.);
#2699=ORIENTED_EDGE('',*,*,#1976,.F.);
#2700=ORIENTED_EDGE('',*,*,#1977,.F.);
#2701=ORIENTED_EDGE('',*,*,#1978,.T.);
#2702=ORIENTED_EDGE('',*,*,#1979,.F.);
#2703=ORIENTED_EDGE('',*,*,#1978,.F.);
#2704=ORIENTED_EDGE('',*,*,#1980,.F.);
#2705=ORIENTED_EDGE('',*,*,#1981,.F.);
#2706=ORIENTED_EDGE('',*,*,#1982,.F.);
#2707=ORIENTED_EDGE('',*,*,#1983,.F.);
#2708=ORIENTED_EDGE('',*,*,#1984,.F.);
#2709=ORIENTED_EDGE('',*,*,#1985,.T.);
#2710=ORIENTED_EDGE('',*,*,#1986,.F.);
#2711=ORIENTED_EDGE('',*,*,#1987,.F.);
#2712=ORIENTED_EDGE('',*,*,#1988,.F.);
#2713=ORIENTED_EDGE('',*,*,#1989,.F.);
#2714=ORIENTED_EDGE('',*,*,#1990,.F.);
#2715=ORIENTED_EDGE('',*,*,#1991,.F.);
#2716=ORIENTED_EDGE('',*,*,#1985,.F.);
#2717=ORIENTED_EDGE('',*,*,#1981,.T.);
#2718=ORIENTED_EDGE('',*,*,#1992,.T.);
#2719=ORIENTED_EDGE('',*,*,#1990,.T.);
#2720=ORIENTED_EDGE('',*,*,#1993,.F.);
#2721=ORIENTED_EDGE('',*,*,#1980,.T.);
#2722=ORIENTED_EDGE('',*,*,#1994,.T.);
#2723=ORIENTED_EDGE('',*,*,#1991,.T.);
#2724=ORIENTED_EDGE('',*,*,#1992,.F.);
#2725=ORIENTED_EDGE('',*,*,#1977,.T.);
#2726=ORIENTED_EDGE('',*,*,#1995,.T.);
#2727=ORIENTED_EDGE('',*,*,#1986,.T.);
#2728=ORIENTED_EDGE('',*,*,#1994,.F.);
#2729=ORIENTED_EDGE('',*,*,#1996,.F.);
#2730=ORIENTED_EDGE('',*,*,#1997,.T.);
#2731=ORIENTED_EDGE('',*,*,#1998,.T.);
#2732=ORIENTED_EDGE('',*,*,#1997,.F.);
#2733=ORIENTED_EDGE('',*,*,#1976,.T.);
#2734=ORIENTED_EDGE('',*,*,#1999,.T.);
#2735=ORIENTED_EDGE('',*,*,#1987,.T.);
#2736=ORIENTED_EDGE('',*,*,#1995,.F.);
#2737=ORIENTED_EDGE('',*,*,#1982,.T.);
#2738=ORIENTED_EDGE('',*,*,#1993,.T.);
#2739=ORIENTED_EDGE('',*,*,#1989,.T.);
#2740=ORIENTED_EDGE('',*,*,#2000,.F.);
#2741=ORIENTED_EDGE('',*,*,#1983,.T.);
#2742=ORIENTED_EDGE('',*,*,#2000,.T.);
#2743=ORIENTED_EDGE('',*,*,#1988,.T.);
#2744=ORIENTED_EDGE('',*,*,#1999,.F.);
#2745=ORIENTED_EDGE('',*,*,#1984,.T.);
#2746=ORIENTED_EDGE('',*,*,#1996,.T.);
#2747=ORIENTED_EDGE('',*,*,#1979,.T.);
#2748=ORIENTED_EDGE('',*,*,#1998,.F.);
#2796=CYLINDRICAL_SURFACE('',#3490,0.338975);
#2959=ADVANCED_FACE('',(#555),#153,.T.);
#2960=ADVANCED_FACE('',(#556),#154,.T.);
#2961=ADVANCED_FACE('',(#557),#385,.T.);
#2962=ADVANCED_FACE('',(#558),#386,.T.);
#2963=ADVANCED_FACE('',(#559),#387,.T.);
#2964=ADVANCED_FACE('',(#560),#2796,.F.);
#2965=ADVANCED_FACE('',(#561),#388,.T.);
#2966=ADVANCED_FACE('',(#562),#389,.T.);
#2967=ADVANCED_FACE('',(#563),#390,.T.);
#2968=ADVANCED_FACE('',(#564,#276),#391,.T.);
#2969=ADVANCED_FACE('',(#565,#277),#392,.F.);
#2987=CLOSED_SHELL('',(#2959,#2960,#2961,#2962,#2963,#2964,#2965,#2966,
#2967,#2968,#2969));
#3482=AXIS2_PLACEMENT_3D('',#5323,#4351,#4352);
#3483=AXIS2_PLACEMENT_3D('',#5324,#4353,#4354);
#3484=AXIS2_PLACEMENT_3D('',#5336,#4356,#4357);
#3485=AXIS2_PLACEMENT_3D('',#5352,#4358,#4359);
#3486=AXIS2_PLACEMENT_3D('',#5354,#4360,#4361);
#3487=AXIS2_PLACEMENT_3D('',#5380,#4363,#4364);
#3488=AXIS2_PLACEMENT_3D('',#5383,#4367,#4368);
#3489=AXIS2_PLACEMENT_3D('',#5385,#4370,#4371);
#3490=AXIS2_PLACEMENT_3D('',#5387,#4373,#4374);
#3491=AXIS2_PLACEMENT_3D('',#5389,#4375,#4376);
#3492=AXIS2_PLACEMENT_3D('',#5392,#4378,#4379);
#3493=AXIS2_PLACEMENT_3D('',#5393,#4380,#4381);
#3494=AXIS2_PLACEMENT_3D('',#5395,#4383,#4384);
#3495=AXIS2_PLACEMENT_3D('',#5397,#4386,#4387);
#3496=AXIS2_PLACEMENT_3D('',#5398,#4388,#4389);
#3497=AXIS2_PLACEMENT_3D('',#5399,#4390,#4391);
#4351=DIRECTION('axis',(0.,0.,1.));
#4352=DIRECTION('refdir',(1.,0.,0.));
#4353=DIRECTION('center_axis',(0.,1.,0.));
#4354=DIRECTION('ref_axis',(1.,0.,0.));
#4355=DIRECTION('',(0.866025403784439,-0.5,1.06057523872491E-16));
#4356=DIRECTION('center_axis',(0.,-1.,0.));
#4357=DIRECTION('ref_axis',(1.,0.,0.));
#4358=DIRECTION('center_axis',(0.,-1.,0.));
#4359=DIRECTION('ref_axis',(1.,0.,0.));
#4360=DIRECTION('center_axis',(0.,1.,0.));
#4361=DIRECTION('ref_axis',(1.,0.,0.));
#4362=DIRECTION('',(-0.866025403784439,-0.5,-1.06057523872491E-16));
#4363=DIRECTION('center_axis',(1.4792020664489E-16,0.,-1.));
#4364=DIRECTION('ref_axis',(-1.,0.,-1.4792020664489E-16));
#4365=DIRECTION('',(0.,1.,0.));
#4366=DIRECTION('',(0.,1.,0.));
#4367=DIRECTION('center_axis',(-0.866025403784439,0.,-0.5));
#4368=DIRECTION('ref_axis',(-0.5,0.,0.866025403784439));
#4369=DIRECTION('',(0.,1.,0.));
#4370=DIRECTION('center_axis',(-0.866025403784439,0.,0.5));
#4371=DIRECTION('ref_axis',(0.5,0.,0.866025403784439));
#4372=DIRECTION('',(0.,1.,0.));
#4373=DIRECTION('center_axis',(0.,1.,0.));
#4374=DIRECTION('ref_axis',(1.,0.,0.));
#4375=DIRECTION('center_axis',(0.,1.,0.));
#4376=DIRECTION('ref_axis',(1.,0.,0.));
#4377=DIRECTION('',(0.,-1.,0.));
#4378=DIRECTION('center_axis',(0.,1.,0.));
#4379=DIRECTION('ref_axis',(1.,0.,0.));
#4380=DIRECTION('center_axis',(-2.95840413289779E-16,0.,1.));
#4381=DIRECTION('ref_axis',(1.,0.,2.95840413289779E-16));
#4382=DIRECTION('',(0.,1.,0.));
#4383=DIRECTION('center_axis',(0.866025403784439,0.,-0.5));
#4384=DIRECTION('ref_axis',(-0.5,0.,-0.866025403784439));
#4385=DIRECTION('',(0.,1.,0.));
#4386=DIRECTION('center_axis',(0.866025403784439,0.,0.5));
#4387=DIRECTION('ref_axis',(0.5,0.,-0.866025403784439));
#4388=DIRECTION('center_axis',(0.,1.,0.));
#4389=DIRECTION('ref_axis',(1.,0.,0.));
#4390=DIRECTION('center_axis',(0.,1.,0.));
#4391=DIRECTION('ref_axis',(1.,0.,0.));
#5323=CARTESIAN_POINT('',(0.,0.,0.));
#5324=CARTESIAN_POINT('Origin',(0.,0.067277284513851,0.));
#5325=CARTESIAN_POINT('',(-0.375277674973257,0.0768195421087395,0.65));
#5326=CARTESIAN_POINT('',(0.375277674973257,0.0768195421087395,0.65));
#5327=CARTESIAN_POINT('Ctrl Pts',(-0.375277674973257,0.0768195421087395,
0.65));
#5328=CARTESIAN_POINT('Ctrl Pts',(1.66533453693773E-13,-0.0315137912242439,
0.65));
#5329=CARTESIAN_POINT('Ctrl Pts',(0.375277674973257,0.0768195421087394,
0.65));
#5330=CARTESIAN_POINT('',(-0.750555349946514,0.0768195421087394,-9.19165206894919E-17));
#5331=CARTESIAN_POINT('Ctrl Pts',(-0.750555349946514,0.0768195421087394,
-9.19165206894919E-17));
#5332=CARTESIAN_POINT('Ctrl Pts',(-0.562916512459802,-0.0315137912242434,
0.325000000000144));
#5333=CARTESIAN_POINT('Ctrl Pts',(-0.375277674973257,0.0768195421087395,
0.65));
#5334=CARTESIAN_POINT('',(-0.6175,-2.77555756156289E-17,-7.5621939847349E-17));
#5335=CARTESIAN_POINT('',(-0.734027674973257,0.067277284513851,-8.98924642641573E-17));
#5336=CARTESIAN_POINT('Origin',(0.,0.,0.));
#5337=CARTESIAN_POINT('',(-0.375277674973257,0.0768195421087395,-0.65));
#5338=CARTESIAN_POINT('Ctrl Pts',(-0.375277674973257,0.0768195421087395,
-0.65));
#5339=CARTESIAN_POINT('Ctrl Pts',(-0.562916512459968,-0.0315137912242437,
-0.324999999999856));
#5340=CARTESIAN_POINT('Ctrl Pts',(-0.750555349946514,0.0768195421087395,
-9.19165206894919E-17));
#5341=CARTESIAN_POINT('',(0.375277674973257,0.0768195421087395,-0.65));
#5342=CARTESIAN_POINT('Ctrl Pts',(0.375277674973257,0.0768195421087395,
-0.65));
#5343=CARTESIAN_POINT('Ctrl Pts',(-1.66144875635155E-13,-0.0315137912242437,
-0.65));
#5344=CARTESIAN_POINT('Ctrl Pts',(-0.375277674973257,0.0768195421087395,
-0.65));
#5345=CARTESIAN_POINT('',(0.750555349946514,0.0768195421087394,0.));
#5346=CARTESIAN_POINT('Ctrl Pts',(0.750555349946514,0.0768195421087394,
0.));
#5347=CARTESIAN_POINT('Ctrl Pts',(0.562916512459802,-0.0315137912242436,
-0.325000000000144));
#5348=CARTESIAN_POINT('Ctrl Pts',(0.375277674973257,0.0768195421087395,
-0.65));
#5349=CARTESIAN_POINT('Ctrl Pts',(0.375277674973257,0.0768195421087394,
0.65));
#5350=CARTESIAN_POINT('Ctrl Pts',(0.562916512459968,-0.0315137912242439,
0.324999999999856));
#5351=CARTESIAN_POINT('Ctrl Pts',(0.750555349946514,0.0768195421087394,
0.));
#5352=CARTESIAN_POINT('Origin',(0.,0.612722715486149,0.));
#5353=CARTESIAN_POINT('',(-0.6175,0.68,-7.5621939847349E-17));
#5354=CARTESIAN_POINT('Origin',(0.,0.68,0.));
#5355=CARTESIAN_POINT('',(-0.750555349946514,0.603180457891261,-9.19165206894919E-17));
#5356=CARTESIAN_POINT('',(-0.734027674973257,0.612722715486149,-8.98924642641573E-17));
#5357=CARTESIAN_POINT('',(-0.375277674973257,0.603180457891261,0.65));
#5358=CARTESIAN_POINT('Ctrl Pts',(-0.375277674973257,0.603180457891261,
0.65));
#5359=CARTESIAN_POINT('Ctrl Pts',(-0.562916512459968,0.711513791224243,
0.324999999999856));
#5360=CARTESIAN_POINT('Ctrl Pts',(-0.750555349946514,0.603180457891261,
-9.19165206894919E-17));
#5361=CARTESIAN_POINT('',(0.375277674973257,0.603180457891261,0.65));
#5362=CARTESIAN_POINT('Ctrl Pts',(0.375277674973257,0.603180457891261,0.65));
#5363=CARTESIAN_POINT('Ctrl Pts',(-1.66755498298699E-13,0.711513791224244,
0.65));
#5364=CARTESIAN_POINT('Ctrl Pts',(-0.375277674973257,0.603180457891261,
0.65));
#5365=CARTESIAN_POINT('',(0.750555349946514,0.603180457891261,0.));
#5366=CARTESIAN_POINT('Ctrl Pts',(0.750555349946514,0.603180457891261,0.));
#5367=CARTESIAN_POINT('Ctrl Pts',(0.562916512459802,0.711513791224244,0.325000000000144));
#5368=CARTESIAN_POINT('Ctrl Pts',(0.375277674973257,0.603180457891261,0.65));
#5369=CARTESIAN_POINT('',(0.375277674973257,0.603180457891261,-0.65));
#5370=CARTESIAN_POINT('Ctrl Pts',(0.375277674973257,0.603180457891261,-0.65));
#5371=CARTESIAN_POINT('Ctrl Pts',(0.562916512459969,0.711513791224244,-0.324999999999856));
#5372=CARTESIAN_POINT('Ctrl Pts',(0.750555349946514,0.603180457891261,0.));
#5373=CARTESIAN_POINT('',(-0.375277674973257,0.603180457891261,-0.65));
#5374=CARTESIAN_POINT('Ctrl Pts',(-0.375277674973257,0.603180457891261,
-0.65));
#5375=CARTESIAN_POINT('Ctrl Pts',(1.66422431391311E-13,0.711513791224244,
-0.65));
#5376=CARTESIAN_POINT('Ctrl Pts',(0.375277674973257,0.603180457891261,-0.65));
#5377=CARTESIAN_POINT('Ctrl Pts',(-0.750555349946514,0.603180457891261,
-9.19165206894919E-17));
#5378=CARTESIAN_POINT('Ctrl Pts',(-0.562916512459802,0.711513791224244,
-0.325000000000144));
#5379=CARTESIAN_POINT('Ctrl Pts',(-0.375277674973257,0.603180457891261,
-0.65));
#5380=CARTESIAN_POINT('Origin',(0.375277674973257,0.,-0.65));
#5381=CARTESIAN_POINT('',(-0.375277674973257,0.,-0.65));
#5382=CARTESIAN_POINT('',(0.375277674973257,0.,-0.65));
#5383=CARTESIAN_POINT('Origin',(-0.375277674973257,0.,-0.65));
#5384=CARTESIAN_POINT('',(-0.750555349946514,0.,-9.19165206894919E-17));
#5385=CARTESIAN_POINT('Origin',(-0.750555349946514,0.,-9.19165206894919E-17));
#5386=CARTESIAN_POINT('',(-0.375277674973257,0.,0.65));
#5387=CARTESIAN_POINT('Origin',(0.,0.,0.));
#5388=CARTESIAN_POINT('',(-0.338975,0.68,4.15124648740974E-17));
#5389=CARTESIAN_POINT('Origin',(0.,0.68,0.));
#5390=CARTESIAN_POINT('',(-0.338975,0.,4.15124648740974E-17));
#5391=CARTESIAN_POINT('',(-0.338975,0.,4.15124648740974E-17));
#5392=CARTESIAN_POINT('Origin',(0.,0.,0.));
#5393=CARTESIAN_POINT('Origin',(-0.375277674973257,0.,0.65));
#5394=CARTESIAN_POINT('',(0.375277674973257,0.,0.65));
#5395=CARTESIAN_POINT('Origin',(0.750555349946514,0.,0.));
#5396=CARTESIAN_POINT('',(0.750555349946514,0.,0.));
#5397=CARTESIAN_POINT('Origin',(0.375277674973257,0.,0.65));
#5398=CARTESIAN_POINT('Origin',(0.,0.68,-1.11022302462516E-16));
#5399=CARTESIAN_POINT('Origin',(0.,0.,-1.11022302462516E-16));
#5434=UNCERTAINTY_MEASURE_WITH_UNIT(LENGTH_MEASURE(0.001),#5459,
'DISTANCE_ACCURACY_VALUE',
'Maximum model space distance between geometric entities at asserted c
onnectivities');
#5435=UNCERTAINTY_MEASURE_WITH_UNIT(LENGTH_MEASURE(0.001),#5459,
'DISTANCE_ACCURACY_VALUE',
'Maximum model space distance between geometric entities at asserted c
onnectivities');
#5457=(
GEOMETRIC_REPRESENTATION_CONTEXT(3)
GLOBAL_UNCERTAINTY_ASSIGNED_CONTEXT((#5434))
GLOBAL_UNIT_ASSIGNED_CONTEXT((#5459,#5461,#5462))
REPRESENTATION_CONTEXT('','3D')
);
#5458=(
GEOMETRIC_REPRESENTATION_CONTEXT(3)
GLOBAL_UNCERTAINTY_ASSIGNED_CONTEXT((#5435))
GLOBAL_UNIT_ASSIGNED_CONTEXT((#5459,#5461,#5462))
REPRESENTATION_CONTEXT('','3D')
);
#5459=(
LENGTH_UNIT()
NAMED_UNIT(*)
SI_UNIT(.CENTI.,.METRE.)
);
#5461=(
NAMED_UNIT(*)
PLANE_ANGLE_UNIT()
SI_UNIT($,.RADIAN.)
);
#5462=(
NAMED_UNIT(*)
SI_UNIT($,.STERADIAN.)
SOLID_ANGLE_UNIT()
);
#5484=SHAPE_DEFINITION_REPRESENTATION(#5520,#5555);
#5520=PRODUCT_DEFINITION_SHAPE('',$,#5578);
#5555=SHAPE_REPRESENTATION('',(#3482),#5457);
#5556=PRODUCT_DEFINITION_CONTEXT('part definition',#5624,'design');
#5578=PRODUCT_DEFINITION('Hex Nut - M8','Hex Nut - M8',#5600,#5556);
#5600=PRODUCT_DEFINITION_FORMATION('',$,#5647);
#5624=APPLICATION_CONTEXT(
'Core Data for Automotive Mechanical Design Process');
#5625=PRODUCT_CONTEXT('part definition',#5624,'mechanical');
#5647=PRODUCT('Hex Nut - M8','Hex Nut - M8','Hex Nut - M8',(#5625));
#5718=COLOUR_RGB('Black',0.12,0.14,0.17);
#5719=FILL_AREA_STYLE_COLOUR('',#5718);
#5720=FILL_AREA_STYLE('',(#5719));
#5721=SURFACE_STYLE_FILL_AREA(#5720);
#5722=SURFACE_SIDE_STYLE('',(#5721));
#5723=SURFACE_STYLE_USAGE(.BOTH.,#5722);
#5724=PRESENTATION_STYLE_ASSIGNMENT((#5723));
ENDSEC;
END-ISO-10303-21;
